ISO-10303-21;
HEADER;
FILE_DESCRIPTION (('STEP AP214'),
    '1' );
FILE_NAME ('large revit.step',
    '2026-10-28T16:30:29',
    ( '' ),
    ( '' ),
    'SwSTEP 2.0',
    'SolidWorks 2025',
    '' );
FILE_SCHEMA (( 'AUTOMOTIVE_DESIGN' ));
ENDSEC;

DATA;
#13=EDGE_LOOP ( 'NONE', ( #3955, #3926, #2198, #6587 ) ) ;
#16=DIRECTION ( 'NONE',  ( 1.000000000000000000, 0.000000000000000000, 0.000000000000000000 ) ) ;
#47=CARTESIAN_POINT ( 'NONE',  ( 4.000000000000003553, 0.000000000000000000, 1.387778780781445676E-14 ) ) ;
#60=CIRCLE ( 'NONE', #2634, 6.000000000000000888 ) ;
#62=DIRECTION ( 'NONE',  ( 0.000000000000000000, 0.000000000000000000, 1.000000000000000000 ) ) ;
#71=CARTESIAN_POINT ( 'NONE',  ( 4.000000000000003553, 0.000000000000000000, 1.387778780781445676E-14 ) ) ;
#94=ORIENTED_EDGE ( 'NONE', *, *, #5676, .T. ) ;
#120=CARTESIAN_POINT ( 'NONE',  ( 36.00000000000000000, 0.000000000000000000, 1.387778780781445676E-14 ) ) ;
#133=DIRECTION ( 'NONE',  ( 0.000000000000000000, -4.440892098500625373E-15, -1.000000000000000000 ) ) ;
#138=AXIS2_PLACEMENT_3D ( 'NONE', #4135, #4211, #3123 ) ;
#152=EDGE_CURVE ( 'NONE', #3617, #6429, #5143, .T. ) ;
#166=DIRECTION ( 'NONE',  ( -1.000000000000000000, 0.000000000000000000, 0.000000000000000000 ) ) ;
#188=AXIS2_PLACEMENT_3D ( 'NONE', #5793, #16, #1672 ) ;
#241=EDGE_LOOP ( 'NONE', ( #6686, #1268 ) ) ;
#254=CARTESIAN_POINT ( 'NONE',  ( 4.000000000000003553, 0.000000000000000000, 1.387778780781445676E-14 ) ) ;
#272=FACE_BOUND ( 'NONE', #4560, .T. ) ;
#277=DIRECTION ( 'NONE',  ( 0.000000000000000000, 0.000000000000000000, -1.000000000000000000 ) ) ;
#284=EDGE_CURVE ( 'NONE', #3833, #7386, #6600, .T. ) ;
#298=ORIENTED_EDGE ( 'NONE', *, *, #6768, .T. ) ;
#311=DIRECTION ( 'NONE',  ( 0.000000000000000000, 0.000000000000000000, -1.000000000000000000 ) ) ;
#357=ORIENTED_EDGE ( 'NONE', *, *, #284, .T. ) ;
#361=CIRCLE ( 'NONE', #1960, 6.000000000000000888 ) ;
#376=CONICAL_SURFACE ( 'NONE', #7132, 7.999999999999986677, 0.7853981633974473908 ) ;
#380=ORIENTED_EDGE ( 'NONE', *, *, #5109, .T. ) ;
#405=ORIENTED_EDGE ( 'NONE', *, *, #591, .F. ) ;
#433=DIRECTION ( 'NONE',  ( -1.000000000000000000, 0.000000000000000000, 0.000000000000000000 ) ) ;
#455=CARTESIAN_POINT ( 'NONE',  ( 37.99999999999998579, 0.000000000000000000, 1.387778780781445676E-14 ) ) ;
#465=ADVANCED_FACE ( 'NONE', ( #3830 ), #376, .T. ) ;
#489=CIRCLE ( 'NONE', #2947, 7.999999999999986677 ) ;
#515=ADVANCED_FACE ( 'NONE', ( #5022 ), #3289, .T. ) ;
#523=CARTESIAN_POINT ( 'NONE',  ( 0.000000000000000000, -4.053118130421075393E-14, 7.999999999999992895 ) ) ;
#548=AXIS2_PLACEMENT_3D ( 'NONE', #47, #5821, #4055 ) ;
#562=ORIENTED_EDGE ( 'NONE', *, *, #5673, .F. ) ;
#591=EDGE_CURVE ( 'NONE', #4871, #7551, #2932, .T. ) ;
#638=ORIENTED_EDGE ( 'NONE', *, *, #5829, .F. ) ;
#640=VERTEX_POINT ( 'NONE', #1124 ) ;
#643=FACE_OUTER_BOUND ( 'NONE', #1378, .T. ) ;
#645=DIRECTION ( 'NONE',  ( 1.000000000000000000, 0.000000000000000000, 0.000000000000000000 ) ) ;
#677=CIRCLE ( 'NONE', #3015, 9.999999999999998224 ) ;
#681=CYLINDRICAL_SURFACE ( 'NONE', #5847, 6.000000000000000888 ) ;
#689=ADVANCED_FACE ( 'NONE', ( #6049 ), #4252, .T. ) ;
#701=ORIENTED_EDGE ( 'NONE', *, *, #4267, .T. ) ;
#704=CARTESIAN_POINT ( 'NONE',  ( 37.99999999999998579, 0.000000000000000000, 1.387778780781445676E-14 ) ) ;
#718=CARTESIAN_POINT ( 'NONE',  ( 36.00000000000000000, 0.000000000000000000, 1.387778780781445676E-14 ) ) ;
#772=EDGE_CURVE ( 'NONE', #7358, #5895, #5896, .T. ) ;
#798=ORIENTED_EDGE ( 'NONE', *, *, #284, .F. ) ;
#800=PRODUCT_DEFINITION_FORMATION_WITH_SPECIFIED_SOURCE ( 'ANY', '', #3413, .NOT_KNOWN. ) ;
#826=CARTESIAN_POINT ( 'NONE',  ( 40.00000000000000000, -4.163336342344337027E-14, 1.387778780781445676E-14 ) ) ;
#842=DIRECTION ( 'NONE',  ( -0.7071067811865482389, 8.659560562354926695E-17, -0.7071067811865469066 ) ) ;
#850=DIRECTION ( 'NONE',  ( 0.000000000000000000, 0.000000000000000000, 1.000000000000000000 ) ) ;
#853=VECTOR ( 'NONE', #5487, 1000.000000000000000 ) ;
#898=FACE_OUTER_BOUND ( 'NONE', #4231, .T. ) ;
#936=ORIENTED_EDGE ( 'NONE', *, *, #152, .F. ) ;
#953=DIRECTION ( 'NONE',  ( 0.7071067811865462405, 0.000000000000000000, -0.7071067811865489050 ) ) ;
#960=FACE_OUTER_BOUND ( 'NONE', #2232, .T. ) ;
#1000=CYLINDRICAL_SURFACE ( 'NONE', #4251, 9.999999999999998224 ) ;
#1019=DIRECTION ( 'NONE',  ( 1.000000000000000000, 0.000000000000000000, 0.000000000000000000 ) ) ;
#1032=ORIENTED_EDGE ( 'NONE', *, *, #2447, .F. ) ;
#1040=DIRECTION ( 'NONE',  ( 0.000000000000000000, 0.000000000000000000, 1.000000000000000000 ) ) ;
#1052=VERTEX_POINT ( 'NONE', #3509 ) ;
#1055=( LENGTH_UNIT ( ) NAMED_UNIT ( * ) SI_UNIT ( .MILLI., .METRE. ) );
#1066=FACE_OUTER_BOUND ( 'NONE', #7346, .T. ) ;
#1102=DIRECTION ( 'NONE',  ( 1.000000000000000000, 0.000000000000000000, 0.000000000000000000 ) ) ;
#1104=DIRECTION ( 'NONE',  ( 0.000000000000000000, 5.329070518200751394E-15, -1.000000000000000000 ) ) ;
#1108=EDGE_LOOP ( 'NONE', ( #3910, #701, #2410, #5551 ) ) ;
#1118=ORIENTED_EDGE ( 'NONE', *, *, #3449, .T. ) ;
#1124=CARTESIAN_POINT ( 'NONE',  ( 0.000000000000000000, 0.000000000000000000, -7.999999999999992895 ) ) ;
#1126=ORIENTED_EDGE ( 'NONE', *, *, #4267, .F. ) ;
#1163=DIRECTION ( 'NONE',  ( -1.000000000000000000, 0.000000000000000000, 0.000000000000000000 ) ) ;
#1169=CARTESIAN_POINT ( 'NONE',  ( 40.00000000000000000, -4.163336342344337027E-14, 8.000000000000000000 ) ) ;
#1182=AXIS2_PLACEMENT_3D ( 'NONE', #5188, #7524, #2266 ) ;
#1215=FACE_OUTER_BOUND ( 'NONE', #6173, .T. ) ;
#1250=CARTESIAN_POINT ( 'NONE',  ( 4.000000000000003553, 1.224646799147353059E-15, -9.999999999999984013 ) ) ;
#1256=CYLINDRICAL_SURFACE ( 'NONE', #1292, 6.000000000000000888 ) ;
#1268=ORIENTED_EDGE ( 'NONE', *, *, #7247, .T. ) ;
#1292=AXIS2_PLACEMENT_3D ( 'NONE', #718, #3612, #7143 ) ;
#1355=( NAMED_UNIT ( * ) PLANE_ANGLE_UNIT ( ) SI_UNIT ( $, .RADIAN. ) );
#1378=EDGE_LOOP ( 'NONE', ( #1607, #2418, #1118, #798 ) ) ;
#1392=AXIS2_PLACEMENT_3D ( 'NONE', #2376, #2452, #3613 ) ;
#1423=CARTESIAN_POINT ( 'NONE',  ( 40.00000000000000000, -4.065364598412548908E-14, -7.999999999999972466 ) ) ;
#1430=EDGE_CURVE ( 'NONE', #640, #6268, #2046, .T. ) ;
#1464=LINE ( 'NONE', #2779, #2883 ) ;
#1505=ORIENTED_EDGE ( 'NONE', *, *, #6254, .T. ) ;
#1522=LINE ( 'NONE', #2189, #4367 ) ;
#1542=EDGE_CURVE ( 'NONE', #6268, #7551, #7360, .T. ) ;
#1548=ORIENTED_EDGE ( 'NONE', *, *, #5676, .F. ) ;
#1550=( NAMED_UNIT ( * ) PLANE_ANGLE_UNIT ( ) SI_UNIT ( $, .RADIAN. ) );
#1579=DIRECTION ( 'NONE',  ( -1.000000000000000000, 0.000000000000000000, 0.000000000000000000 ) ) ;
#1584=LINE ( 'NONE', #1169, #7216 ) ;
#1601=ADVANCED_BREP_SHAPE_REPRESENTATION ( '', ( #6414, #1914 ), #5969 ) ;
#1607=ORIENTED_EDGE ( 'NONE', *, *, #5457, .F. ) ;
#1628=DIRECTION ( 'NONE',  ( 0.000000000000000000, 0.000000000000000000, -1.000000000000000000 ) ) ;
#1637=FACE_BOUND ( 'NONE', #4497, .T. ) ;
#1643=EDGE_CURVE ( 'NONE', #6174, #2698, #1584, .T. ) ;
#1672=DIRECTION ( 'NONE',  ( 0.000000000000000000, 0.000000000000000000, -1.000000000000000000 ) ) ;
#1737=EDGE_LOOP ( 'NONE', ( #6956, #7125, #7575, #562 ) ) ;
#1743=ORIENTED_EDGE ( 'NONE', *, *, #1643, .F. ) ;
#1749=CARTESIAN_POINT ( 'NONE',  ( 0.000000000000000000, 0.000000000000000000, 0.000000000000000000 ) ) ;
#1771=EDGE_LOOP ( 'NONE', ( #1884, #2354 ) ) ;
#1782=CIRCLE ( 'NONE', #2399, 7.999999999999986677 ) ;
#1785=CIRCLE ( 'NONE', #4751, 9.999999999999998224 ) ;
#1799=DIRECTION ( 'NONE',  ( -1.000000000000000000, 0.000000000000000000, 0.000000000000000000 ) ) ;
#1864=DIRECTION ( 'NONE',  ( 1.000000000000000000, 0.000000000000000000, 0.000000000000000000 ) ) ;
#1884=ORIENTED_EDGE ( 'NONE', *, *, #2621, .T. ) ;
#1900=AXIS2_PLACEMENT_3D ( 'NONE', #3195, #2228, #6258 ) ;
#1914=AXIS2_PLACEMENT_3D ( 'NONE', #1749, #62, #1864 ) ;
#1916=APPLICATION_CONTEXT ( 'automotive_design' ) ;
#1918=ORIENTED_EDGE ( 'NONE', *, *, #772, .F. ) ;
#1919=VERTEX_POINT ( 'NONE', #3712 ) ;
#1946=DIRECTION ( 'NONE',  ( -1.000000000000000000, 0.000000000000000000, 0.000000000000000000 ) ) ;
#1960=AXIS2_PLACEMENT_3D ( 'NONE', #6870, #3916, #1628 ) ;
#2029=CIRCLE ( 'NONE', #188, 9.999999999999998224 ) ;
#2046=CIRCLE ( 'NONE', #4642, 7.999999999999992895 ) ;
#2060=DIRECTION ( 'NONE',  ( -1.000000000000000000, -0.000000000000000000, -0.000000000000000000 ) ) ;
#2096=DIRECTION ( 'NONE',  ( 0.7071067811865462405, 8.659560562354950115E-17, 0.7071067811865489050 ) ) ;
#2123=ORIENTED_EDGE ( 'NONE', *, *, #1430, .T. ) ;
#2129=DIRECTION ( 'NONE',  ( 0.000000000000000000, 0.000000000000000000, -1.000000000000000000 ) ) ;
#2189=CARTESIAN_POINT ( 'NONE',  ( 2.000000000000001776, -4.163336342344337027E-14, -9.999999999999998224 ) ) ;
#2198=ORIENTED_EDGE ( 'NONE', *, *, #5673, .T. ) ;
#2228=DIRECTION ( 'NONE',  ( 1.000000000000000000, 0.000000000000000000, 0.000000000000000000 ) ) ;
#2232=EDGE_LOOP ( 'NONE', ( #94, #298, #2657, #6478 ) ) ;
#2266=DIRECTION ( 'NONE',  ( 0.000000000000000000, 0.000000000000000000, -1.000000000000000000 ) ) ;
#2268=DIRECTION ( 'NONE',  ( -1.000000000000000000, -0.000000000000000000, -0.000000000000000000 ) ) ;
#2354=ORIENTED_EDGE ( 'NONE', *, *, #6948, .T. ) ;
#2376=CARTESIAN_POINT ( 'NONE',  ( 36.00000000000000000, 0.000000000000000000, 1.387778780781445676E-14 ) ) ;
#2382=DIRECTION ( 'NONE',  ( 1.000000000000000000, 0.000000000000000000, 0.000000000000000000 ) ) ;
#2399=AXIS2_PLACEMENT_3D ( 'NONE', #6497, #6420, #5877 ) ;
#2410=ORIENTED_EDGE ( 'NONE', *, *, #4035, .T. ) ;
#2418=ORIENTED_EDGE ( 'NONE', *, *, #772, .T. ) ;
#2447=EDGE_CURVE ( 'NONE', #3833, #7358, #4635, .T. ) ;
#2452=DIRECTION ( 'NONE',  ( 1.000000000000000000, 0.000000000000000000, 0.000000000000000000 ) ) ;
#2476=( LENGTH_UNIT ( ) NAMED_UNIT ( * ) SI_UNIT ( .MILLI., .METRE. ) );
#2481=UNCERTAINTY_MEASURE_WITH_UNIT (LENGTH_MEASURE( 1.000000000000000082E-05 ), #2476, 'distance_accuracy_value', 'NONE');
#2506=EDGE_LOOP ( 'NONE', ( #3320, #3127, #6602, #1126 ) ) ;
#2520=SHAPE_REPRESENTATION_RELATIONSHIP ( 'NONE' , 'NONE' ,  #2538, #1601 ) ;
#2538=SHAPE_REPRESENTATION ( 'large revit', ( #1914 ), #5969 ) ;
#2559=CARTESIAN_POINT ( 'NONE',  ( 0.000000000000000000, 0.000000000000000000, 0.000000000000000000 ) ) ;
#2576=LINE ( 'NONE', #1423, #4970 ) ;
#2577=FACE_OUTER_BOUND ( 'NONE', #13, .T. ) ;
#2578=VERTEX_POINT ( 'NONE', #3687 ) ;
#2621=EDGE_CURVE ( 'NONE', #4871, #3617, #4327, .T. ) ;
#2625=( NAMED_UNIT ( * ) SI_UNIT ( $, .STERADIAN. ) SOLID_ANGLE_UNIT ( ) );
#2633=CIRCLE ( 'NONE', #3870, 6.000000000000000888 ) ;
#2634=AXIS2_PLACEMENT_3D ( 'NONE', #4040, #1102, #5804 ) ;
#2657=ORIENTED_EDGE ( 'NONE', *, *, #3250, .T. ) ;
#2672=DIRECTION ( 'NONE',  ( 0.000000000000000000, 0.000000000000000000, -1.000000000000000000 ) ) ;
#2689=CARTESIAN_POINT ( 'NONE',  ( 36.00000000000000000, -4.163336342344337027E-14, 10.00000000000001243 ) ) ;
#2698=VERTEX_POINT ( 'NONE', #3136 ) ;
#2735=CARTESIAN_POINT ( 'NONE',  ( 4.000000000000003553, 0.000000000000000000, 1.387778780781445676E-14 ) ) ;
#2752=CIRCLE ( 'NONE', #3622, 7.999999999999992895 ) ;
#2765=AXIS2_PLACEMENT_3D ( 'NONE', #704, #4359, #133 ) ;
#2779=CARTESIAN_POINT ( 'NONE',  ( 40.00000000000000000, -4.040871662429601878E-14, -9.999999999999984013 ) ) ;
#2797=FACE_OUTER_BOUND ( 'NONE', #1737, .T. ) ;
#2863=VECTOR ( 'NONE', #1163, 1000.000000000000000 ) ;
#2869=CONICAL_SURFACE ( 'NONE', #7172, 9.999999999999998224, 0.7853981633974501664 ) ;
#2883=VECTOR ( 'NONE', #433, 1000.000000000000000 ) ;
#2900=CARTESIAN_POINT ( 'NONE',  ( 40.00000000000000000, -4.163336342344337027E-14, 10.00000000000001243 ) ) ;
#2932=LINE ( 'NONE', #5752, #5047 ) ;
#2947=AXIS2_PLACEMENT_3D ( 'NONE', #5722, #1019, #6339 ) ;
#2994=CIRCLE ( 'NONE', #1392, 9.999999999999998224 ) ;
#3015=AXIS2_PLACEMENT_3D ( 'NONE', #455, #2268, #1104 ) ;
#3092=CARTESIAN_POINT ( 'NONE',  ( 2.000000000000001776, -4.163336342344337027E-14, 0.000000000000000000 ) ) ;
#3123=DIRECTION ( 'NONE',  ( 0.000000000000000000, 0.000000000000000000, -1.000000000000000000 ) ) ;
#3126=CONICAL_SURFACE ( 'NONE', #5466, 7.999999999999986677, 0.7853981633974473908 ) ;
#3127=ORIENTED_EDGE ( 'NONE', *, *, #3553, .F. ) ;
#3136=CARTESIAN_POINT ( 'NONE',  ( 37.99999999999998579, -4.163336342344337027E-14, 10.00000000000001243 ) ) ;
#3156=ORIENTED_EDGE ( 'NONE', *, *, #2447, .T. ) ;
#3160=DIRECTION ( 'NONE',  ( 1.000000000000000000, 0.000000000000000000, 0.000000000000000000 ) ) ;
#3189=ORIENTED_EDGE ( 'NONE', *, *, #7247, .F. ) ;
#3195=CARTESIAN_POINT ( 'NONE',  ( 36.00000000000000000, 0.000000000000000000, 1.387778780781445676E-14 ) ) ;
#3250=EDGE_CURVE ( 'NONE', #1919, #5113, #5415, .T. ) ;
#3289=CYLINDRICAL_SURFACE ( 'NONE', #5785, 9.999999999999998224 ) ;
#3311=ORIENTED_EDGE ( 'NONE', *, *, #3449, .F. ) ;
#3320=ORIENTED_EDGE ( 'NONE', *, *, #5109, .F. ) ;
#3331=DIRECTION ( 'NONE',  ( 0.000000000000000000, 0.000000000000000000, -1.000000000000000000 ) ) ;
#3372=PLANE ( 'NONE',  #7183 ) ;
#3413=PRODUCT ( 'large revit', 'large revit', '', ( #5823 ) ) ;
#3449=EDGE_CURVE ( 'NONE', #5895, #7386, #361, .T. ) ;
#3451=CLOSED_SHELL ( 'NONE', ( #465, #6068, #4341, #7279, #6235, #515, #5086, #6426, #7290, #7328, #689, #7017, #7004, #6664 ) ) ;
#3478=SHAPE_DEFINITION_REPRESENTATION ( #3534, #2538 ) ;
#3509=CARTESIAN_POINT ( 'NONE',  ( 37.99999999999998579, -4.040871662429601878E-14, -9.999999999999984013 ) ) ;
#3534=PRODUCT_DEFINITION_SHAPE ( 'NONE', 'NONE',  #6635 ) ;
#3553=EDGE_CURVE ( 'NONE', #6174, #2578, #489, .T. ) ;
#3574=CARTESIAN_POINT ( 'NONE',  ( 4.000000000000003553, 7.347880794884120722E-16, -5.999999999999986677 ) ) ;
#3576=CARTESIAN_POINT ( 'NONE',  ( 36.00000000000000000, 0.000000000000000000, 1.387778780781445676E-14 ) ) ;
#3593=ORIENTED_EDGE ( 'NONE', *, *, #7127, .F. ) ;
#3610=CYLINDRICAL_SURFACE ( 'NONE', #5093, 9.999999999999998224 ) ;
#3612=DIRECTION ( 'NONE',  ( -1.000000000000000000, 0.000000000000000000, 0.000000000000000000 ) ) ;
#3613=DIRECTION ( 'NONE',  ( 0.000000000000000000, 0.000000000000000000, -1.000000000000000000 ) ) ;
#3617=VERTEX_POINT ( 'NONE', #1250 ) ;
#3622=AXIS2_PLACEMENT_3D ( 'NONE', #7068, #5911, #5949 ) ;
#3687=CARTESIAN_POINT ( 'NONE',  ( 40.00000000000000000, -4.053118130421075393E-14, -7.999999999999972466 ) ) ;
#3712=CARTESIAN_POINT ( 'NONE',  ( 36.00000000000000000, -4.040871662429601878E-14, -9.999999999999984013 ) ) ;
#3762=CARTESIAN_POINT ( 'NONE',  ( 2.000000000000001776, -4.040871662429601878E-14, 9.999999999999998224 ) ) ;
#3790=DIRECTION ( 'NONE',  ( -1.000000000000000000, 0.000000000000000000, 0.000000000000000000 ) ) ;
#3830=FACE_OUTER_BOUND ( 'NONE', #4339, .T. ) ;
#3833=VERTEX_POINT ( 'NONE', #5023 ) ;
#3836=CARTESIAN_POINT ( 'NONE',  ( 0.000000000000000000, 0.000000000000000000, 0.000000000000000000 ) ) ;
#3870=AXIS2_PLACEMENT_3D ( 'NONE', #120, #2382, #4850 ) ;
#3894=PLANE ( 'NONE',  #5334 ) ;
#3910=ORIENTED_EDGE ( 'NONE', *, *, #6768, .F. ) ;
#3916=DIRECTION ( 'NONE',  ( 1.000000000000000000, 0.000000000000000000, 0.000000000000000000 ) ) ;
#3920=DIRECTION ( 'NONE',  ( 0.000000000000000000, 0.000000000000000000, -1.000000000000000000 ) ) ;
#3926=ORIENTED_EDGE ( 'NONE', *, *, #1430, .F. ) ;
#3939=DIRECTION ( 'NONE',  ( 0.000000000000000000, 0.000000000000000000, 1.000000000000000000 ) ) ;
#3955=ORIENTED_EDGE ( 'NONE', *, *, #1542, .F. ) ;
#3967=ORIENTED_EDGE ( 'NONE', *, *, #2621, .F. ) ;
#4035=EDGE_CURVE ( 'NONE', #2698, #5113, #5936, .T. ) ;
#4040=CARTESIAN_POINT ( 'NONE',  ( 4.000000000000003553, 0.000000000000000000, 1.387778780781445676E-14 ) ) ;
#4055=DIRECTION ( 'NONE',  ( 0.000000000000000000, 0.000000000000000000, -1.000000000000000000 ) ) ;
#4135=CARTESIAN_POINT ( 'NONE',  ( 40.00000000000000000, -4.163336342344337027E-14, 1.387778780781445676E-14 ) ) ;
#4150=ORIENTED_EDGE ( 'NONE', *, *, #4194, .T. ) ;
#4194=EDGE_CURVE ( 'NONE', #7551, #6429, #1785, .T. ) ;
#4211=DIRECTION ( 'NONE',  ( 1.000000000000000000, 0.000000000000000000, 0.000000000000000000 ) ) ;
#4231=EDGE_LOOP ( 'NONE', ( #2123, #1505 ) ) ;
#4251=AXIS2_PLACEMENT_3D ( 'NONE', #6232, #7499, #1040 ) ;
#4252=PLANE ( 'NONE',  #138 ) ;
#4267=EDGE_CURVE ( 'NONE', #1052, #2698, #7310, .T. ) ;
#4327=CIRCLE ( 'NONE', #6154, 9.999999999999998224 ) ;
#4337=CARTESIAN_POINT ( 'NONE',  ( 4.000000000000003553, 0.000000000000000000, 6.000000000000015099 ) ) ;
#4339=EDGE_LOOP ( 'NONE', ( #3189, #380, #1548, #1743 ) ) ;
#4341=ADVANCED_FACE ( 'NONE', ( #960 ), #1000, .T. ) ;
#4359=DIRECTION ( 'NONE',  ( -1.000000000000000000, -0.000000000000000000, -0.000000000000000000 ) ) ;
#4365=ORIENTED_EDGE ( 'NONE', *, *, #6538, .T. ) ;
#4367=VECTOR ( 'NONE', #953, 999.9999999999998863 ) ;
#4413=FACE_OUTER_BOUND ( 'NONE', #1108, .T. ) ;
#4441=DIRECTION ( 'NONE',  ( 0.000000000000000000, 0.000000000000000000, 1.000000000000000000 ) ) ;
#4455=CARTESIAN_POINT ( 'NONE',  ( 40.00000000000000000, -4.163336342344337027E-14, 8.000000000000000000 ) ) ;
#4479=CARTESIAN_POINT ( 'NONE',  ( 40.00000000000000000, -4.163336342344337027E-14, 1.387778780781445676E-14 ) ) ;
#4485=( GEOMETRIC_REPRESENTATION_CONTEXT ( 3 ) GLOBAL_UNCERTAINTY_ASSIGNED_CONTEXT ( ( #5411 ) ) GLOBAL_UNIT_ASSIGNED_CONTEXT ( ( #1055, #1550, #6247 ) ) REPRESENTATION_CONTEXT ( 'NONE', 'WORKASPACE' ) );
#4488=DIRECTION ( 'NONE',  ( 1.000000000000000000, 0.000000000000000000, 0.000000000000000000 ) ) ;
#4497=EDGE_LOOP ( 'NONE', ( #3156, #4670 ) ) ;
#4560=EDGE_LOOP ( 'NONE', ( #3593, #3311 ) ) ;
#4566=CARTESIAN_POINT ( 'NONE',  ( 2.000000000000001776, -2.465190328815661892E-29, 9.999999999999998224 ) ) ;
#4570=VECTOR ( 'NONE', #166, 1000.000000000000000 ) ;
#4635=CIRCLE ( 'NONE', #1182, 6.000000000000000888 ) ;
#4642=AXIS2_PLACEMENT_3D ( 'NONE', #2559, #2060, #2129 ) ;
#4670=ORIENTED_EDGE ( 'NONE', *, *, #5457, .T. ) ;
#4683=AXIS2_PLACEMENT_3D ( 'NONE', #3576, #645, #5343 ) ;
#4695=CARTESIAN_POINT ( 'NONE',  ( 36.00000000000000000, 0.000000000000000000, 1.387778780781445676E-14 ) ) ;
#4751=AXIS2_PLACEMENT_3D ( 'NONE', #3092, #7236, #277 ) ;
#4767=CARTESIAN_POINT ( 'NONE',  ( 36.00000000000000000, 0.000000000000000000, 6.000000000000015099 ) ) ;
#4850=DIRECTION ( 'NONE',  ( 0.000000000000000000, 0.000000000000000000, -1.000000000000000000 ) ) ;
#4871=VERTEX_POINT ( 'NONE', #6317 ) ;
#4934=DIRECTION ( 'NONE',  ( 0.000000000000000000, 0.000000000000000000, -1.000000000000000000 ) ) ;
#4955=CARTESIAN_POINT ( 'NONE',  ( 36.00000000000000000, 7.347880794884120722E-16, -5.999999999999986677 ) ) ;
#4970=VECTOR ( 'NONE', #842, 999.9999999999998863 ) ;
#4979=CONICAL_SURFACE ( 'NONE', #6576, 9.999999999999998224, 0.7853981633974501664 ) ;
#4998=DIRECTION ( 'NONE',  ( 0.000000000000000000, 0.000000000000000000, 1.000000000000000000 ) ) ;
#5022=FACE_OUTER_BOUND ( 'NONE', #5423, .T. ) ;
#5023=CARTESIAN_POINT ( 'NONE',  ( 36.00000000000000000, 0.000000000000000000, 6.000000000000015099 ) ) ;
#5026=CARTESIAN_POINT ( 'NONE',  ( 2.000000000000001776, 1.224646799147405913E-15, -9.999999999999998224 ) ) ;
#5047=VECTOR ( 'NONE', #7474, 1000.000000000000000 ) ;
#5086=ADVANCED_FACE ( 'NONE', ( #272, #5544 ), #3894, .T. ) ;
#5093=AXIS2_PLACEMENT_3D ( 'NONE', #71, #1799, #6989 ) ;
#5109=EDGE_CURVE ( 'NONE', #2578, #1052, #2576, .T. ) ;
#5113=VERTEX_POINT ( 'NONE', #2689 ) ;
#5127=EDGE_LOOP ( 'NONE', ( #1918, #1032, #357, #6848 ) ) ;
#5143=LINE ( 'NONE', #6412, #7250 ) ;
#5188=CARTESIAN_POINT ( 'NONE',  ( 36.00000000000000000, 0.000000000000000000, 1.387778780781445676E-14 ) ) ;
#5315=ORIENTED_EDGE ( 'NONE', *, *, #152, .T. ) ;
#5334=AXIS2_PLACEMENT_3D ( 'NONE', #6769, #7272, #311 ) ;
#5343=DIRECTION ( 'NONE',  ( 0.000000000000000000, 0.000000000000000000, -1.000000000000000000 ) ) ;
#5381=DIRECTION ( 'NONE',  ( -1.000000000000000000, 0.000000000000000000, 0.000000000000000000 ) ) ;
#5411=UNCERTAINTY_MEASURE_WITH_UNIT (LENGTH_MEASURE( 1.000000000000000082E-05 ), #1055, 'distance_accuracy_value', 'NONE');
#5415=CIRCLE ( 'NONE', #4683, 9.999999999999998224 ) ;
#5423=EDGE_LOOP ( 'NONE', ( #936, #3967, #5497, #4150 ) ) ;
#5457=EDGE_CURVE ( 'NONE', #7358, #3833, #2633, .T. ) ;
#5466=AXIS2_PLACEMENT_3D ( 'NONE', #6054, #3790, #850 ) ;
#5487=DIRECTION ( 'NONE',  ( -1.000000000000000000, 0.000000000000000000, 0.000000000000000000 ) ) ;
#5497=ORIENTED_EDGE ( 'NONE', *, *, #591, .T. ) ;
#5544=FACE_OUTER_BOUND ( 'NONE', #1771, .T. ) ;
#5551=ORIENTED_EDGE ( 'NONE', *, *, #5829, .T. ) ;
#5588=STYLED_ITEM('',(#7652),#6414);
#5630=DIRECTION ( 'NONE',  ( -1.000000000000000000, 0.000000000000000000, 0.000000000000000000 ) ) ;
#5673=EDGE_CURVE ( 'NONE', #640, #6429, #1522, .T. ) ;
#5676=EDGE_CURVE ( 'NONE', #2698, #1052, #677, .T. ) ;
#5686=DIRECTION ( 'NONE',  ( 1.000000000000000000, 0.000000000000000000, 0.000000000000000000 ) ) ;
#5722=CARTESIAN_POINT ( 'NONE',  ( 40.00000000000000000, -4.163336342344337027E-14, 1.387778780781445676E-14 ) ) ;
#5752=CARTESIAN_POINT ( 'NONE',  ( 4.000000000000003553, 0.000000000000000000, 10.00000000000001243 ) ) ;
#5785=AXIS2_PLACEMENT_3D ( 'NONE', #2735, #5630, #3939 ) ;
#5793=CARTESIAN_POINT ( 'NONE',  ( 2.000000000000001776, -4.163336342344337027E-14, 0.000000000000000000 ) ) ;
#5804=DIRECTION ( 'NONE',  ( 0.000000000000000000, 0.000000000000000000, -1.000000000000000000 ) ) ;
#5821=DIRECTION ( 'NONE',  ( 1.000000000000000000, 0.000000000000000000, 0.000000000000000000 ) ) ;
#5823=PRODUCT_CONTEXT ( 'NONE', #1916, 'mechanical' ) ;
#5829=EDGE_CURVE ( 'NONE', #5113, #1919, #2994, .T. ) ;
#5844=DIRECTION ( 'NONE',  ( 0.000000000000000000, 0.000000000000000000, 1.000000000000000000 ) ) ;
#5847=AXIS2_PLACEMENT_3D ( 'NONE', #4695, #5381, #5844 ) ;
#5873=DIRECTION ( 'NONE',  ( -1.000000000000000000, 0.000000000000000000, 0.000000000000000000 ) ) ;
#5877=DIRECTION ( 'NONE',  ( 0.000000000000000000, 0.000000000000000000, -1.000000000000000000 ) ) ;
#5895=VERTEX_POINT ( 'NONE', #3574 ) ;
#5896=LINE ( 'NONE', #6625, #4570 ) ;
#5911=DIRECTION ( 'NONE',  ( -1.000000000000000000, -0.000000000000000000, -0.000000000000000000 ) ) ;
#5936=LINE ( 'NONE', #2900, #2863 ) ;
#5949=DIRECTION ( 'NONE',  ( 0.000000000000000000, 8.881784197001252323E-16, -1.000000000000000000 ) ) ;
#5951=FACE_OUTER_BOUND ( 'NONE', #5127, .T. ) ;
#5969=( GEOMETRIC_REPRESENTATION_CONTEXT ( 3 ) GLOBAL_UNCERTAINTY_ASSIGNED_CONTEXT ( ( #2481 ) ) GLOBAL_UNIT_ASSIGNED_CONTEXT ( ( #2476, #1355, #2625 ) ) REPRESENTATION_CONTEXT ( 'NONE', 'WORKASPACE' ) );
#6049=FACE_OUTER_BOUND ( 'NONE', #241, .T. ) ;
#6054=CARTESIAN_POINT ( 'NONE',  ( 40.00000000000000000, -4.163336342344337027E-14, 1.387778780781445676E-14 ) ) ;
#6068=ADVANCED_FACE ( 'NONE', ( #2797 ), #2869, .T. ) ;
#6080=MECHANICAL_DESIGN_GEOMETRIC_PRESENTATION_REPRESENTATION('',(#5588),#4485);
#6154=AXIS2_PLACEMENT_3D ( 'NONE', #254, #4488, #3331 ) ;
#6168=DIRECTION ( 'NONE',  ( 1.000000000000000000, 0.000000000000000000, 0.000000000000000000 ) ) ;
#6173=EDGE_LOOP ( 'NONE', ( #6667, #5315, #4365, #405 ) ) ;
#6174=VERTEX_POINT ( 'NONE', #4455 ) ;
#6232=CARTESIAN_POINT ( 'NONE',  ( 40.00000000000000000, -4.163336342344337027E-14, 1.387778780781445676E-14 ) ) ;
#6235=ADVANCED_FACE ( 'NONE', ( #1215 ), #3610, .T. ) ;
#6247=( NAMED_UNIT ( * ) SI_UNIT ( $, .STERADIAN. ) SOLID_ANGLE_UNIT ( ) );
#6254=EDGE_CURVE ( 'NONE', #6268, #640, #2752, .T. ) ;
#6258=DIRECTION ( 'NONE',  ( 0.000000000000000000, 0.000000000000000000, -1.000000000000000000 ) ) ;
#6268=VERTEX_POINT ( 'NONE', #523 ) ;
#6317=CARTESIAN_POINT ( 'NONE',  ( 4.000000000000003553, 0.000000000000000000, 10.00000000000001243 ) ) ;
#6339=DIRECTION ( 'NONE',  ( 0.000000000000000000, 0.000000000000000000, -1.000000000000000000 ) ) ;
#6383=PLANE ( 'NONE',  #1900 ) ;
#6412=CARTESIAN_POINT ( 'NONE',  ( 4.000000000000003553, 1.224646799147353059E-15, -9.999999999999984013 ) ) ;
#6414=MANIFOLD_SOLID_BREP ( 'Chamfer1', #3451 ) ;
#6420=DIRECTION ( 'NONE',  ( 1.000000000000000000, 0.000000000000000000, 0.000000000000000000 ) ) ;
#6426=ADVANCED_FACE ( 'NONE', ( #898 ), #3372, .F. ) ;
#6429=VERTEX_POINT ( 'NONE', #5026 ) ;
#6455=AXIS2_PLACEMENT_3D ( 'NONE', #826, #1946, #4998 ) ;
#6478=ORIENTED_EDGE ( 'NONE', *, *, #4035, .F. ) ;
#6491=PRODUCT_DEFINITION_CONTEXT ( 'detailed design', #7027, 'design' ) ;
#6497=CARTESIAN_POINT ( 'NONE',  ( 40.00000000000000000, -4.163336342344337027E-14, 1.387778780781445676E-14 ) ) ;
#6538=EDGE_CURVE ( 'NONE', #6429, #7551, #2029, .T. ) ;
#6576=AXIS2_PLACEMENT_3D ( 'NONE', #7233, #3160, #4934 ) ;
#6587=ORIENTED_EDGE ( 'NONE', *, *, #4194, .F. ) ;
#6598=FACE_OUTER_BOUND ( 'NONE', #2506, .T. ) ;
#6600=LINE ( 'NONE', #4767, #853 ) ;
#6602=ORIENTED_EDGE ( 'NONE', *, *, #1643, .T. ) ;
#6606=CYLINDRICAL_SURFACE ( 'NONE', #6455, 9.999999999999998224 ) ;
#6625=CARTESIAN_POINT ( 'NONE',  ( 36.00000000000000000, 7.347880794884120722E-16, -5.999999999999986677 ) ) ;
#6635=PRODUCT_DEFINITION ( 'UNKNOWN', '', #800, #6491 ) ;
#6664=ADVANCED_FACE ( 'NONE', ( #6598 ), #3126, .T. ) ;
#6667=ORIENTED_EDGE ( 'NONE', *, *, #6948, .F. ) ;
#6686=ORIENTED_EDGE ( 'NONE', *, *, #3553, .T. ) ;
#6768=EDGE_CURVE ( 'NONE', #1052, #1919, #1464, .T. ) ;
#6769=CARTESIAN_POINT ( 'NONE',  ( 4.000000000000003553, 0.000000000000000000, 1.387778780781445676E-14 ) ) ;
#6848=ORIENTED_EDGE ( 'NONE', *, *, #7127, .T. ) ;
#6870=CARTESIAN_POINT ( 'NONE',  ( 4.000000000000003553, 0.000000000000000000, 1.387778780781445676E-14 ) ) ;
#6947=DIRECTION ( 'NONE',  ( -0.7071067811865482389, 0.000000000000000000, 0.7071067811865469066 ) ) ;
#6948=EDGE_CURVE ( 'NONE', #3617, #4871, #7058, .T. ) ;
#6956=ORIENTED_EDGE ( 'NONE', *, *, #6254, .F. ) ;
#6989=DIRECTION ( 'NONE',  ( 0.000000000000000000, 0.000000000000000000, 1.000000000000000000 ) ) ;
#7004=ADVANCED_FACE ( 'NONE', ( #2577 ), #4979, .T. ) ;
#7017=ADVANCED_FACE ( 'NONE', ( #1637, #1066 ), #6383, .F. ) ;
#7027=APPLICATION_CONTEXT ( 'automotive_design' ) ;
#7058=CIRCLE ( 'NONE', #548, 9.999999999999998224 ) ;
#7068=CARTESIAN_POINT ( 'NONE',  ( 0.000000000000000000, 0.000000000000000000, 0.000000000000000000 ) ) ;
#7088=VECTOR ( 'NONE', #2096, 999.9999999999998863 ) ;
#7125=ORIENTED_EDGE ( 'NONE', *, *, #1542, .T. ) ;
#7127=EDGE_CURVE ( 'NONE', #7386, #5895, #60, .T. ) ;
#7132=AXIS2_PLACEMENT_3D ( 'NONE', #4479, #1579, #4441 ) ;
#7143=DIRECTION ( 'NONE',  ( 0.000000000000000000, 0.000000000000000000, 1.000000000000000000 ) ) ;
#7172=AXIS2_PLACEMENT_3D ( 'NONE', #7523, #5686, #3920 ) ;
#7183=AXIS2_PLACEMENT_3D ( 'NONE', #3836, #6168, #2672 ) ;
#7216=VECTOR ( 'NONE', #6947, 999.9999999999998863 ) ;
#7233=CARTESIAN_POINT ( 'NONE',  ( 2.000000000000001776, -4.163336342344337027E-14, 0.000000000000000000 ) ) ;
#7236=DIRECTION ( 'NONE',  ( 1.000000000000000000, 0.000000000000000000, 0.000000000000000000 ) ) ;
#7247=EDGE_CURVE ( 'NONE', #2578, #6174, #1782, .T. ) ;
#7250=VECTOR ( 'NONE', #5873, 1000.000000000000000 ) ;
#7272=DIRECTION ( 'NONE',  ( 1.000000000000000000, 0.000000000000000000, 0.000000000000000000 ) ) ;
#7279=ADVANCED_FACE ( 'NONE', ( #643 ), #1256, .T. ) ;
#7290=ADVANCED_FACE ( 'NONE', ( #5951 ), #681, .T. ) ;
#7310=CIRCLE ( 'NONE', #2765, 9.999999999999998224 ) ;
#7328=ADVANCED_FACE ( 'NONE', ( #4413 ), #6606, .T. ) ;
#7346=EDGE_LOOP ( 'NONE', ( #638, #7512 ) ) ;
#7358=VERTEX_POINT ( 'NONE', #4955 ) ;
#7360=LINE ( 'NONE', #3762, #7088 ) ;
#7386=VERTEX_POINT ( 'NONE', #4337 ) ;
#7474=DIRECTION ( 'NONE',  ( -1.000000000000000000, 0.000000000000000000, 0.000000000000000000 ) ) ;
#7499=DIRECTION ( 'NONE',  ( -1.000000000000000000, 0.000000000000000000, 0.000000000000000000 ) ) ;
#7512=ORIENTED_EDGE ( 'NONE', *, *, #3250, .F. ) ;
#7523=CARTESIAN_POINT ( 'NONE',  ( 2.000000000000001776, -4.163336342344337027E-14, 0.000000000000000000 ) ) ;
#7524=DIRECTION ( 'NONE',  ( 1.000000000000000000, 0.000000000000000000, 0.000000000000000000 ) ) ;
#7551=VERTEX_POINT ( 'NONE', #4566 ) ;
#7575=ORIENTED_EDGE ( 'NONE', *, *, #6538, .F. ) ;
#7646=COLOUR_RGB('Off White',0.89,0.88,0.83);
#7647=FILL_AREA_STYLE_COLOUR('',#7646);
#7648=FILL_AREA_STYLE('',(#7647));
#7649=SURFACE_STYLE_FILL_AREA(#7648);
#7650=SURFACE_SIDE_STYLE('',(#7649));
#7651=SURFACE_STYLE_USAGE(.BOTH.,#7650);
#7652=PRESENTATION_STYLE_ASSIGNMENT((#7651));
ENDSEC;
END-ISO-10303-21;
